ISO-10303-21;
HEADER;
/* Generated by software containing ST-Developer
 * from STEP Tools, Inc. (www.steptools.com) 
 */

FILE_DESCRIPTION(
/* description */ (''),
/* implementation_level */ '2;1');

FILE_NAME(
/* name */ 'Ball_01.step',
/* time_stamp */ '2026-10-06T12:47:13-07:00',
/* author */ (''),
/* organization */ (''),
/* preprocessor_version */ 'ST-DEVELOPER v20.2',
/* originating_system */ 'Autodesk Translation Framework v15.15.0.0',
/* authorisation */ '');

FILE_SCHEMA (('AUTOMOTIVE_DESIGN { 1 0 10303 214 3 1 1 }'));
ENDSEC;

DATA;
#10=MECHANICAL_DESIGN_GEOMETRIC_PRESENTATION_REPRESENTATION('',(#72),#42667);
#48=SPHERICAL_SURFACE('',#4304,10.);
#54=SHAPE_REPRESENTATION_RELATIONSHIP('SRR','None',#42707,#63);
#63=ADVANCED_BREP_SHAPE_REPRESENTATION('',(#81),#42663);
#72=STYLED_ITEM('',(#42756),#81);
#81=MANIFOLD_SOLID_BREP('Body1',#4037);
#570=CIRCLE('',#4303,9.1643052178268);
#746=FACE_OUTER_BOUND('',#955,.T.);
#747=FACE_OUTER_BOUND('',#956,.T.);
#955=EDGE_LOOP('',(#3288));
#956=EDGE_LOOP('',(#3289));
#1760=VERTEX_POINT('',#33572);
#2295=EDGE_CURVE('',#1760,#1760,#570,.T.);
#3288=ORIENTED_EDGE('',*,*,#2295,.T.);
#3289=ORIENTED_EDGE('',*,*,#2295,.F.);
#3808=PLANE('',#4302);
#3942=ADVANCED_FACE('',(#746),#3808,.T.);
#3943=ADVANCED_FACE('',(#747),#48,.T.);
#4037=CLOSED_SHELL('',(#3942,#3943));
#4301=AXIS2_PLACEMENT_3D('',#33570,#4903,#4904);
#4302=AXIS2_PLACEMENT_3D('',#33571,#4905,#4906);
#4303=AXIS2_PLACEMENT_3D('',#33573,#4907,#4908);
#4304=AXIS2_PLACEMENT_3D('',#33574,#4909,#4910);
#4903=DIRECTION('axis',(0.,0.,1.));
#4904=DIRECTION('refdir',(1.,0.,0.));
#4905=DIRECTION('center_axis',(0.,1.,0.));
#4906=DIRECTION('ref_axis',(0.,0.,1.));
#4907=DIRECTION('center_axis',(0.,1.,0.));
#4908=DIRECTION('ref_axis',(1.,0.,0.));
#4909=DIRECTION('center_axis',(1.22464679914735E-16,0.,1.));
#4910=DIRECTION('ref_axis',(1.,0.,-6.12323399573677E-17));
#33570=CARTESIAN_POINT('',(0.,0.,0.));
#33571=CARTESIAN_POINT('Origin',(0.,-4.0019382647053,0.));
#33572=CARTESIAN_POINT('',(0.,-4.0019382647053,9.1643052178268));
#33573=CARTESIAN_POINT('Origin',(0.,-4.0019382647053,0.));
#33574=CARTESIAN_POINT('Origin',(0.,0.,0.));
#42652=UNCERTAINTY_MEASURE_WITH_UNIT(LENGTH_MEASURE(0.01),#42668,
'DISTANCE_ACCURACY_VALUE',
'Maximum model space distance between geometric entities at asserted c
onnectivities');
#42656=UNCERTAINTY_MEASURE_WITH_UNIT(LENGTH_MEASURE(0.01),#42668,
'DISTANCE_ACCURACY_VALUE',
'Maximum model space distance between geometric entities at asserted c
onnectivities');
#42663=(
GEOMETRIC_REPRESENTATION_CONTEXT(3)
GLOBAL_UNCERTAINTY_ASSIGNED_CONTEXT((#42652))
GLOBAL_UNIT_ASSIGNED_CONTEXT((#42668,#42670,#42671))
REPRESENTATION_CONTEXT('','3D')
);
#42667=(
GEOMETRIC_REPRESENTATION_CONTEXT(3)
GLOBAL_UNCERTAINTY_ASSIGNED_CONTEXT((#42656))
GLOBAL_UNIT_ASSIGNED_CONTEXT((#42668,#42670,#42671))
REPRESENTATION_CONTEXT('','3D')
);
#42668=(
LENGTH_UNIT()
NAMED_UNIT(*)
SI_UNIT(.MILLI.,.METRE.)
);
#42670=(
NAMED_UNIT(*)
PLANE_ANGLE_UNIT()
SI_UNIT($,.RADIAN.)
);
#42671=(
NAMED_UNIT(*)
SI_UNIT($,.STERADIAN.)
SOLID_ANGLE_UNIT()
);
#42678=SHAPE_DEFINITION_REPRESENTATION(#42688,#42707);
#42688=PRODUCT_DEFINITION_SHAPE('',$,#42718);
#42707=SHAPE_REPRESENTATION('',(#4301),#42663);
#42711=PRODUCT_DEFINITION_CONTEXT('part definition',#42743,'design');
#42718=PRODUCT_DEFINITION('Ball_01','Ball_01',#42728,#42711);
#42728=PRODUCT_DEFINITION_FORMATION('',$,#42751);
#42743=APPLICATION_CONTEXT(
'Core Data for Automotive Mechanical Design Process');
#42744=PRODUCT_CONTEXT('part definition',#42743,'mechanical');
#42751=PRODUCT('Ball_01','Ball_01',$,(#42744));
#42756=PRESENTATION_STYLE_ASSIGNMENT((#42758));
#42758=SURFACE_STYLE_USAGE(.BOTH.,#42760);
#42760=SURFACE_SIDE_STYLE('',(#42762));
#42762=SURFACE_STYLE_FILL_AREA(#42764);
#42764=FILL_AREA_STYLE('Opaque(160,160,160)',(#42766));
#42766=FILL_AREA_STYLE_COLOUR('Opaque(160,160,160)',#42768);
#42768=COLOUR_RGB('Opaque(160,160,160)', 0.09019608, 0.27058824, 0.51372549);
ENDSEC;
END-ISO-10303-21;
